ISO-10303-21;
HEADER;
/* Generated by software containing ST-Developer
 * from STEP Tools, Inc. (www.steptools.com) 
 */

FILE_DESCRIPTION(
/* description */ ('Spur gear reduction stage 2-1 on bearing plates'),
/* implementation_level */ '2;1');

FILE_NAME(
/* name */ 'Cap Screw - M4x16.step',
/* time_stamp */ '2026-10-28T03:22:07-07:00',
/* author */ (''),
/* organization */ (''),
/* preprocessor_version */ 'ST-DEVELOPER v20.2',
/* originating_system */ 'Autodesk Translation Framework v15.17.0.0',
/* authorisation */ '');

FILE_SCHEMA (('AUTOMOTIVE_DESIGN { 1 0 10303 214 3 1 1 }'));
ENDSEC;

DATA;
#10=MECHANICAL_DESIGN_GEOMETRIC_PRESENTATION_REPRESENTATION('',(#985),#53909);
#831=ORIENTED_CLOSED_SHELL('',*,#11312,.F.);
#848=CONICAL_SURFACE('',#12418,0.325,0.785398163397448);
#849=CONICAL_SURFACE('',#12422,0.335,0.785398163397448);
#850=CONICAL_SURFACE('',#12426,0.21,0.463647609000806);
#851=CONICAL_SURFACE('',#12430,0.18,0.785398163397448);
#860=BREP_WITH_VOIDS('Body1',#11311,(#831));
#884=SHAPE_REPRESENTATION_RELATIONSHIP('SRR','None',#54113,#927);
#927=ADVANCED_BREP_SHAPE_REPRESENTATION('',(#860),#53887);
#985=STYLED_ITEM('',(#54404),#860);
#1196=FACE_BOUND('',#2555,.T.);
#1347=PLANE('',#12416);
#1348=PLANE('',#12424);
#1349=PLANE('',#12432);
#1350=PLANE('',#12433);
#1351=PLANE('',#12434);
#1352=PLANE('',#12435);
#1353=PLANE('',#12436);
#1354=PLANE('',#12437);
#1355=PLANE('',#12438);
#1356=PLANE('',#12439);
#1357=PLANE('',#12440);
#1766=FACE_OUTER_BOUND('',#2550,.T.);
#1767=FACE_OUTER_BOUND('',#2551,.T.);
#1768=FACE_OUTER_BOUND('',#2552,.T.);
#1769=FACE_OUTER_BOUND('',#2553,.T.);
#1770=FACE_OUTER_BOUND('',#2554,.T.);
#1771=FACE_OUTER_BOUND('',#2556,.T.);
#1772=FACE_OUTER_BOUND('',#2557,.T.);
#1773=FACE_OUTER_BOUND('',#2558,.T.);
#1774=FACE_OUTER_BOUND('',#2559,.T.);
#1775=FACE_OUTER_BOUND('',#2560,.T.);
#1776=FACE_OUTER_BOUND('',#2561,.T.);
#1777=FACE_OUTER_BOUND('',#2562,.T.);
#1778=FACE_OUTER_BOUND('',#2563,.T.);
#1779=FACE_OUTER_BOUND('',#2564,.T.);
#1780=FACE_OUTER_BOUND('',#2565,.T.);
#1781=FACE_OUTER_BOUND('',#2566,.T.);
#1782=FACE_OUTER_BOUND('',#2567,.T.);
#2550=EDGE_LOOP('',(#8418));
#2551=EDGE_LOOP('',(#8419,#8420,#8421,#8422));
#2552=EDGE_LOOP('',(#8423,#8424,#8425,#8426));
#2553=EDGE_LOOP('',(#8427,#8428,#8429,#8430));
#2554=EDGE_LOOP('',(#8431));
#2555=EDGE_LOOP('',(#8432));
#2556=EDGE_LOOP('',(#8433,#8434,#8435,#8436));
#2557=EDGE_LOOP('',(#8437,#8438,#8439,#8440));
#2558=EDGE_LOOP('',(#8441,#8442,#8443,#8444));
#2559=EDGE_LOOP('',(#8445));
#2560=EDGE_LOOP('',(#8446,#8447,#8448,#8449));
#2561=EDGE_LOOP('',(#8450,#8451,#8452,#8453));
#2562=EDGE_LOOP('',(#8454,#8455,#8456,#8457));
#2563=EDGE_LOOP('',(#8458,#8459,#8460,#8461));
#2564=EDGE_LOOP('',(#8462,#8463,#8464,#8465));
#2565=EDGE_LOOP('',(#8466,#8467,#8468,#8469));
#2566=EDGE_LOOP('',(#8470,#8471,#8472,#8473,#8474,#8475));
#2567=EDGE_LOOP('',(#8476,#8477,#8478,#8479,#8480,#8481));
#3169=LINE('',#17817,#3810);
#3170=LINE('',#17821,#3811);
#3171=LINE('',#17825,#3812);
#3172=LINE('',#17832,#3813);
#3173=LINE('',#17836,#3814);
#3174=LINE('',#17840,#3815);
#3175=LINE('',#17845,#3816);
#3176=LINE('',#17847,#3817);
#3177=LINE('',#17849,#3818);
#3178=LINE('',#17850,#3819);
#3179=LINE('',#17853,#3820);
#3180=LINE('',#17855,#3821);
#3181=LINE('',#17856,#3822);
#3182=LINE('',#17859,#3823);
#3183=LINE('',#17861,#3824);
#3184=LINE('',#17862,#3825);
#3185=LINE('',#17865,#3826);
#3186=LINE('',#17867,#3827);
#3187=LINE('',#17868,#3828);
#3188=LINE('',#17871,#3829);
#3189=LINE('',#17873,#3830);
#3190=LINE('',#17874,#3831);
#3191=LINE('',#17876,#3832);
#3192=LINE('',#17877,#3833);
#3810=VECTOR('',#14402,0.325);
#3811=VECTOR('',#14407,0.35);
#3812=VECTOR('',#14412,0.335);
#3813=VECTOR('',#14421,0.21);
#3814=VECTOR('',#14426,0.2);
#3815=VECTOR('',#14431,0.18);
#3816=VECTOR('',#14436,1.);
#3817=VECTOR('',#14437,1.);
#3818=VECTOR('',#14438,1.);
#3819=VECTOR('',#14439,1.);
#3820=VECTOR('',#14442,1.);
#3821=VECTOR('',#14443,1.);
#3822=VECTOR('',#14444,1.);
#3823=VECTOR('',#14447,1.);
#3824=VECTOR('',#14448,1.);
#3825=VECTOR('',#14449,1.);
#3826=VECTOR('',#14452,1.);
#3827=VECTOR('',#14453,1.);
#3828=VECTOR('',#14454,1.);
#3829=VECTOR('',#14457,1.);
#3830=VECTOR('',#14458,1.);
#3831=VECTOR('',#14459,1.);
#3832=VECTOR('',#14462,1.);
#3833=VECTOR('',#14463,1.);
#4568=CIRCLE('',#12417,0.3);
#4569=CIRCLE('',#12419,0.35);
#4570=CIRCLE('',#12421,0.35);
#4571=CIRCLE('',#12423,0.32);
#4572=CIRCLE('',#12425,0.22);
#4573=CIRCLE('',#12427,0.1954);
#4574=CIRCLE('',#12429,0.1954);
#4575=CIRCLE('',#12431,0.16);
#5154=VERTEX_POINT('',#17812);
#5155=VERTEX_POINT('',#17815);
#5156=VERTEX_POINT('',#17819);
#5157=VERTEX_POINT('',#17823);
#5158=VERTEX_POINT('',#17827);
#5159=VERTEX_POINT('',#17830);
#5160=VERTEX_POINT('',#17834);
#5161=VERTEX_POINT('',#17838);
#5162=VERTEX_POINT('',#17843);
#5163=VERTEX_POINT('',#17844);
#5164=VERTEX_POINT('',#17846);
#5165=VERTEX_POINT('',#17848);
#5166=VERTEX_POINT('',#17852);
#5167=VERTEX_POINT('',#17854);
#5168=VERTEX_POINT('',#17858);
#5169=VERTEX_POINT('',#17860);
#5170=VERTEX_POINT('',#17864);
#5171=VERTEX_POINT('',#17866);
#5172=VERTEX_POINT('',#17870);
#5173=VERTEX_POINT('',#17872);
#6351=EDGE_CURVE('',#5154,#5154,#4568,.T.);
#6352=EDGE_CURVE('',#5155,#5155,#4569,.T.);
#6353=EDGE_CURVE('',#5155,#5154,#3169,.T.);
#6354=EDGE_CURVE('',#5156,#5156,#4570,.T.);
#6355=EDGE_CURVE('',#5156,#5155,#3170,.T.);
#6356=EDGE_CURVE('',#5157,#5157,#4571,.T.);
#6357=EDGE_CURVE('',#5157,#5156,#3171,.T.);
#6358=EDGE_CURVE('',#5158,#5158,#4572,.T.);
#6359=EDGE_CURVE('',#5159,#5159,#4573,.F.);
#6360=EDGE_CURVE('',#5159,#5158,#3172,.T.);
#6361=EDGE_CURVE('',#5160,#5160,#4574,.F.);
#6362=EDGE_CURVE('',#5160,#5159,#3173,.T.);
#6363=EDGE_CURVE('',#5161,#5161,#4575,.T.);
#6364=EDGE_CURVE('',#5161,#5160,#3174,.T.);
#6365=EDGE_CURVE('',#5162,#5163,#3175,.T.);
#6366=EDGE_CURVE('',#5163,#5164,#3176,.T.);
#6367=EDGE_CURVE('',#5164,#5165,#3177,.T.);
#6368=EDGE_CURVE('',#5162,#5165,#3178,.T.);
#6369=EDGE_CURVE('',#5163,#5166,#3179,.T.);
#6370=EDGE_CURVE('',#5166,#5167,#3180,.T.);
#6371=EDGE_CURVE('',#5167,#5164,#3181,.T.);
#6372=EDGE_CURVE('',#5166,#5168,#3182,.T.);
#6373=EDGE_CURVE('',#5168,#5169,#3183,.T.);
#6374=EDGE_CURVE('',#5169,#5167,#3184,.T.);
#6375=EDGE_CURVE('',#5168,#5170,#3185,.T.);
#6376=EDGE_CURVE('',#5170,#5171,#3186,.T.);
#6377=EDGE_CURVE('',#5171,#5169,#3187,.T.);
#6378=EDGE_CURVE('',#5170,#5172,#3188,.T.);
#6379=EDGE_CURVE('',#5172,#5173,#3189,.T.);
#6380=EDGE_CURVE('',#5173,#5171,#3190,.T.);
#6381=EDGE_CURVE('',#5172,#5162,#3191,.T.);
#6382=EDGE_CURVE('',#5165,#5173,#3192,.T.);
#8418=ORIENTED_EDGE('',*,*,#6351,.F.);
#8419=ORIENTED_EDGE('',*,*,#6352,.F.);
#8420=ORIENTED_EDGE('',*,*,#6353,.T.);
#8421=ORIENTED_EDGE('',*,*,#6351,.T.);
#8422=ORIENTED_EDGE('',*,*,#6353,.F.);
#8423=ORIENTED_EDGE('',*,*,#6354,.F.);
#8424=ORIENTED_EDGE('',*,*,#6355,.T.);
#8425=ORIENTED_EDGE('',*,*,#6352,.T.);
#8426=ORIENTED_EDGE('',*,*,#6355,.F.);
#8427=ORIENTED_EDGE('',*,*,#6356,.F.);
#8428=ORIENTED_EDGE('',*,*,#6357,.T.);
#8429=ORIENTED_EDGE('',*,*,#6354,.T.);
#8430=ORIENTED_EDGE('',*,*,#6357,.F.);
#8431=ORIENTED_EDGE('',*,*,#6356,.T.);
#8432=ORIENTED_EDGE('',*,*,#6358,.F.);
#8433=ORIENTED_EDGE('',*,*,#6359,.F.);
#8434=ORIENTED_EDGE('',*,*,#6360,.T.);
#8435=ORIENTED_EDGE('',*,*,#6358,.T.);
#8436=ORIENTED_EDGE('',*,*,#6360,.F.);
#8437=ORIENTED_EDGE('',*,*,#6361,.F.);
#8438=ORIENTED_EDGE('',*,*,#6362,.T.);
#8439=ORIENTED_EDGE('',*,*,#6359,.T.);
#8440=ORIENTED_EDGE('',*,*,#6362,.F.);
#8441=ORIENTED_EDGE('',*,*,#6363,.F.);
#8442=ORIENTED_EDGE('',*,*,#6364,.T.);
#8443=ORIENTED_EDGE('',*,*,#6361,.T.);
#8444=ORIENTED_EDGE('',*,*,#6364,.F.);
#8445=ORIENTED_EDGE('',*,*,#6363,.T.);
#8446=ORIENTED_EDGE('',*,*,#6365,.T.);
#8447=ORIENTED_EDGE('',*,*,#6366,.T.);
#8448=ORIENTED_EDGE('',*,*,#6367,.T.);
#8449=ORIENTED_EDGE('',*,*,#6368,.F.);
#8450=ORIENTED_EDGE('',*,*,#6369,.T.);
#8451=ORIENTED_EDGE('',*,*,#6370,.T.);
#8452=ORIENTED_EDGE('',*,*,#6371,.T.);
#8453=ORIENTED_EDGE('',*,*,#6366,.F.);
#8454=ORIENTED_EDGE('',*,*,#6372,.T.);
#8455=ORIENTED_EDGE('',*,*,#6373,.T.);
#8456=ORIENTED_EDGE('',*,*,#6374,.T.);
#8457=ORIENTED_EDGE('',*,*,#6370,.F.);
#8458=ORIENTED_EDGE('',*,*,#6375,.T.);
#8459=ORIENTED_EDGE('',*,*,#6376,.T.);
#8460=ORIENTED_EDGE('',*,*,#6377,.T.);
#8461=ORIENTED_EDGE('',*,*,#6373,.F.);
#8462=ORIENTED_EDGE('',*,*,#6378,.T.);
#8463=ORIENTED_EDGE('',*,*,#6379,.T.);
#8464=ORIENTED_EDGE('',*,*,#6380,.T.);
#8465=ORIENTED_EDGE('',*,*,#6376,.F.);
#8466=ORIENTED_EDGE('',*,*,#6381,.T.);
#8467=ORIENTED_EDGE('',*,*,#6368,.T.);
#8468=ORIENTED_EDGE('',*,*,#6382,.T.);
#8469=ORIENTED_EDGE('',*,*,#6379,.F.);
#8470=ORIENTED_EDGE('',*,*,#6381,.F.);
#8471=ORIENTED_EDGE('',*,*,#6378,.F.);
#8472=ORIENTED_EDGE('',*,*,#6375,.F.);
#8473=ORIENTED_EDGE('',*,*,#6372,.F.);
#8474=ORIENTED_EDGE('',*,*,#6369,.F.);
#8475=ORIENTED_EDGE('',*,*,#6365,.F.);
#8476=ORIENTED_EDGE('',*,*,#6382,.F.);
#8477=ORIENTED_EDGE('',*,*,#6367,.F.);
#8478=ORIENTED_EDGE('',*,*,#6371,.F.);
#8479=ORIENTED_EDGE('',*,*,#6374,.F.);
#8480=ORIENTED_EDGE('',*,*,#6377,.F.);
#8481=ORIENTED_EDGE('',*,*,#6380,.F.);
#10524=CYLINDRICAL_SURFACE('',#12420,0.35);
#10525=CYLINDRICAL_SURFACE('',#12428,0.1954);
#10886=ADVANCED_FACE('',(#1766),#1347,.T.);
#10887=ADVANCED_FACE('',(#1767),#848,.T.);
#10888=ADVANCED_FACE('',(#1768),#10524,.T.);
#10889=ADVANCED_FACE('',(#1769),#849,.T.);
#10890=ADVANCED_FACE('',(#1770,#1196),#1348,.T.);
#10891=ADVANCED_FACE('',(#1771),#850,.T.);
#10892=ADVANCED_FACE('',(#1772),#10525,.T.);
#10893=ADVANCED_FACE('',(#1773),#851,.T.);
#10894=ADVANCED_FACE('',(#1774),#1349,.T.);
#10895=ADVANCED_FACE('',(#1775),#1350,.F.);
#10896=ADVANCED_FACE('',(#1776),#1351,.F.);
#10897=ADVANCED_FACE('',(#1777),#1352,.F.);
#10898=ADVANCED_FACE('',(#1778),#1353,.F.);
#10899=ADVANCED_FACE('',(#1779),#1354,.F.);
#10900=ADVANCED_FACE('',(#1780),#1355,.F.);
#10901=ADVANCED_FACE('',(#1781),#1356,.F.);
#10902=ADVANCED_FACE('',(#1782),#1357,.F.);
#11311=CLOSED_SHELL('',(#10886,#10887,#10888,#10889,#10890,#10891,#10892,
#10893,#10894));
#11312=CLOSED_SHELL('',(#10895,#10896,#10897,#10898,#10899,#10900,#10901,
#10902));
#12415=AXIS2_PLACEMENT_3D('',#17810,#14392,#14393);
#12416=AXIS2_PLACEMENT_3D('',#17811,#14394,#14395);
#12417=AXIS2_PLACEMENT_3D('',#17813,#14396,#14397);
#12418=AXIS2_PLACEMENT_3D('',#17814,#14398,#14399);
#12419=AXIS2_PLACEMENT_3D('',#17816,#14400,#14401);
#12420=AXIS2_PLACEMENT_3D('',#17818,#14403,#14404);
#12421=AXIS2_PLACEMENT_3D('',#17820,#14405,#14406);
#12422=AXIS2_PLACEMENT_3D('',#17822,#14408,#14409);
#12423=AXIS2_PLACEMENT_3D('',#17824,#14410,#14411);
#12424=AXIS2_PLACEMENT_3D('',#17826,#14413,#14414);
#12425=AXIS2_PLACEMENT_3D('',#17828,#14415,#14416);
#12426=AXIS2_PLACEMENT_3D('',#17829,#14417,#14418);
#12427=AXIS2_PLACEMENT_3D('',#17831,#14419,#14420);
#12428=AXIS2_PLACEMENT_3D('',#17833,#14422,#14423);
#12429=AXIS2_PLACEMENT_3D('',#17835,#14424,#14425);
#12430=AXIS2_PLACEMENT_3D('',#17837,#14427,#14428);
#12431=AXIS2_PLACEMENT_3D('',#17839,#14429,#14430);
#12432=AXIS2_PLACEMENT_3D('',#17841,#14432,#14433);
#12433=AXIS2_PLACEMENT_3D('',#17842,#14434,#14435);
#12434=AXIS2_PLACEMENT_3D('',#17851,#14440,#14441);
#12435=AXIS2_PLACEMENT_3D('',#17857,#14445,#14446);
#12436=AXIS2_PLACEMENT_3D('',#17863,#14450,#14451);
#12437=AXIS2_PLACEMENT_3D('',#17869,#14455,#14456);
#12438=AXIS2_PLACEMENT_3D('',#17875,#14460,#14461);
#12439=AXIS2_PLACEMENT_3D('',#17878,#14464,#14465);
#12440=AXIS2_PLACEMENT_3D('',#17879,#14466,#14467);
#14392=DIRECTION('axis',(0.,0.,1.));
#14393=DIRECTION('refdir',(1.,0.,0.));
#14394=DIRECTION('center_axis',(0.,1.,0.));
#14395=DIRECTION('ref_axis',(0.,0.,1.));
#14396=DIRECTION('center_axis',(0.,-1.,0.));
#14397=DIRECTION('ref_axis',(1.,0.,0.));
#14398=DIRECTION('center_axis',(0.,-1.,0.));
#14399=DIRECTION('ref_axis',(1.,0.,0.));
#14400=DIRECTION('center_axis',(0.,-1.,0.));
#14401=DIRECTION('ref_axis',(1.,0.,0.));
#14402=DIRECTION('',(0.707106781186547,0.707106781186548,8.65956056235493E-17));
#14403=DIRECTION('center_axis',(0.,-1.,0.));
#14404=DIRECTION('ref_axis',(1.,0.,0.));
#14405=DIRECTION('center_axis',(0.,-1.,0.));
#14406=DIRECTION('ref_axis',(1.,0.,0.));
#14407=DIRECTION('',(0.,1.,0.));
#14408=DIRECTION('center_axis',(0.,1.,0.));
#14409=DIRECTION('ref_axis',(1.,0.,0.));
#14410=DIRECTION('center_axis',(0.,-1.,0.));
#14411=DIRECTION('ref_axis',(1.,0.,0.));
#14412=DIRECTION('',(-0.707106781186547,0.707106781186548,-8.65956056235493E-17));
#14413=DIRECTION('center_axis',(0.,-1.,0.));
#14414=DIRECTION('ref_axis',(0.,0.,-1.));
#14415=DIRECTION('center_axis',(0.,-1.,0.));
#14416=DIRECTION('ref_axis',(1.,0.,0.));
#14417=DIRECTION('center_axis',(0.,1.,0.));
#14418=DIRECTION('ref_axis',(1.,0.,0.));
#14419=DIRECTION('center_axis',(0.,1.,0.));
#14420=DIRECTION('ref_axis',(1.,0.,0.));
#14421=DIRECTION('',(-0.447213595499958,0.894427190999916,-5.47678698264203E-17));
#14422=DIRECTION('center_axis',(0.,-1.,0.));
#14423=DIRECTION('ref_axis',(1.,0.,0.));
#14424=DIRECTION('center_axis',(0.,1.,0.));
#14425=DIRECTION('ref_axis',(1.,0.,0.));
#14426=DIRECTION('',(0.,1.,0.));
#14427=DIRECTION('center_axis',(0.,1.,0.));
#14428=DIRECTION('ref_axis',(1.,0.,0.));
#14429=DIRECTION('center_axis',(0.,-1.,0.));
#14430=DIRECTION('ref_axis',(1.,0.,0.));
#14431=DIRECTION('',(-0.707106781186547,0.707106781186548,-8.65956056235493E-17));
#14432=DIRECTION('center_axis',(0.,-1.,0.));
#14433=DIRECTION('ref_axis',(0.,0.,-1.));
#14434=DIRECTION('center_axis',(0.866025403784439,0.,-0.5));
#14435=DIRECTION('ref_axis',(0.5,0.,0.866025403784439));
#14436=DIRECTION('',(-0.5,0.,-0.866025403784439));
#14437=DIRECTION('',(0.,-1.,0.));
#14438=DIRECTION('',(0.5,0.,0.866025403784439));
#14439=DIRECTION('',(0.,-1.,0.));
#14440=DIRECTION('center_axis',(1.60246890531964E-16,0.,-1.));
#14441=DIRECTION('ref_axis',(1.,0.,1.60246890531964E-16));
#14442=DIRECTION('',(-1.,0.,-1.60246890531964E-16));
#14443=DIRECTION('',(0.,-1.,0.));
#14444=DIRECTION('',(1.,0.,1.60246890531964E-16));
#14445=DIRECTION('center_axis',(-0.866025403784439,0.,-0.5));
#14446=DIRECTION('ref_axis',(0.5,0.,-0.866025403784439));
#14447=DIRECTION('',(-0.5,0.,0.866025403784439));
#14448=DIRECTION('',(0.,-1.,0.));
#14449=DIRECTION('',(0.5,0.,-0.866025403784439));
#14450=DIRECTION('center_axis',(-0.866025403784439,0.,0.5));
#14451=DIRECTION('ref_axis',(-0.5,0.,-0.866025403784439));
#14452=DIRECTION('',(0.5,0.,0.866025403784439));
#14453=DIRECTION('',(0.,-1.,0.));
#14454=DIRECTION('',(-0.5,0.,-0.866025403784439));
#14455=DIRECTION('center_axis',(-1.60246890531964E-16,0.,1.));
#14456=DIRECTION('ref_axis',(-1.,0.,-1.60246890531964E-16));
#14457=DIRECTION('',(1.,0.,1.60246890531964E-16));
#14458=DIRECTION('',(0.,-1.,0.));
#14459=DIRECTION('',(-1.,0.,-1.60246890531964E-16));
#14460=DIRECTION('center_axis',(0.866025403784439,0.,0.5));
#14461=DIRECTION('ref_axis',(-0.5,0.,0.866025403784439));
#14462=DIRECTION('',(0.5,0.,-0.866025403784439));
#14463=DIRECTION('',(-0.5,0.,0.866025403784439));
#14464=DIRECTION('center_axis',(0.,1.,0.));
#14465=DIRECTION('ref_axis',(1.,0.,0.));
#14466=DIRECTION('center_axis',(0.,-1.,0.));
#14467=DIRECTION('ref_axis',(0.,0.,-1.));
#17810=CARTESIAN_POINT('',(0.,0.,0.));
#17811=CARTESIAN_POINT('Origin',(0.3,0.4,0.));
#17812=CARTESIAN_POINT('',(-0.3,0.4,-3.67394039744206E-17));
#17813=CARTESIAN_POINT('Origin',(0.,0.4,0.));
#17814=CARTESIAN_POINT('Origin',(0.,0.375,0.));
#17815=CARTESIAN_POINT('',(-0.35,0.35,-4.28626379701573E-17));
#17816=CARTESIAN_POINT('Origin',(0.,0.35,0.));
#17817=CARTESIAN_POINT('',(-0.325,0.375,-3.9801020972289E-17));
#17818=CARTESIAN_POINT('Origin',(0.,0.19,0.));
#17819=CARTESIAN_POINT('',(-0.35,0.03,-4.28626379701574E-17));
#17820=CARTESIAN_POINT('Origin',(0.,0.03,0.));
#17821=CARTESIAN_POINT('',(-0.35,0.19,-4.28626379701574E-17));
#17822=CARTESIAN_POINT('Origin',(0.,0.0149999999999999,0.));
#17823=CARTESIAN_POINT('',(-0.32,-3.29597460435593E-17,-3.91886975727153E-17));
#17824=CARTESIAN_POINT('Origin',(0.,0.,0.));
#17825=CARTESIAN_POINT('',(-0.335,0.0149999999999999,-4.10256677714363E-17));
#17826=CARTESIAN_POINT('Origin',(0.22,0.,0.));
#17827=CARTESIAN_POINT('',(-0.22,-6.93889390390723E-18,-2.69422295812418E-17));
#17828=CARTESIAN_POINT('Origin',(0.,0.,0.));
#17829=CARTESIAN_POINT('Origin',(0.,-0.02,0.));
#17830=CARTESIAN_POINT('',(-0.1954,-0.0492,2.39295984553393E-17));
#17831=CARTESIAN_POINT('Origin',(0.,-0.0492,0.));
#17832=CARTESIAN_POINT('',(-0.21,-0.02,-2.57175827820944E-17));
#17833=CARTESIAN_POINT('Origin',(0.,-0.8,0.));
#17834=CARTESIAN_POINT('',(-0.1954,-1.5646,2.39295984553393E-17));
#17835=CARTESIAN_POINT('Origin',(0.,-1.5646,0.));
#17836=CARTESIAN_POINT('',(-0.1954,-0.8,-2.39295984553393E-17));
#17837=CARTESIAN_POINT('Origin',(0.,-1.58,0.));
#17838=CARTESIAN_POINT('',(-0.16,-1.6,-1.95943487863577E-17));
#17839=CARTESIAN_POINT('Origin',(0.,-1.6,0.));
#17840=CARTESIAN_POINT('',(-0.18,-1.58,-2.20436423846524E-17));
#17841=CARTESIAN_POINT('Origin',(0.,-1.6,0.));
#17842=CARTESIAN_POINT('Origin',(0.0866025403784439,-0.4,-0.15));
#17843=CARTESIAN_POINT('',(0.173205080756888,-0.4,0.));
#17844=CARTESIAN_POINT('',(0.0866025403784439,-0.4,-0.15));
#17845=CARTESIAN_POINT('',(0.173205080756888,-0.4,0.));
#17846=CARTESIAN_POINT('',(0.0866025403784439,-0.64,-0.15));
#17847=CARTESIAN_POINT('',(0.0866025403784439,-0.4,-0.15));
#17848=CARTESIAN_POINT('',(0.173205080756888,-0.64,0.));
#17849=CARTESIAN_POINT('',(0.173205080756888,-0.64,0.));
#17850=CARTESIAN_POINT('',(0.173205080756888,-0.4,0.));
#17851=CARTESIAN_POINT('Origin',(-0.0866025403784438,-0.4,-0.15));
#17852=CARTESIAN_POINT('',(-0.0866025403784438,-0.4,-0.15));
#17853=CARTESIAN_POINT('',(0.0866025403784439,-0.4,-0.15));
#17854=CARTESIAN_POINT('',(-0.0866025403784438,-0.64,-0.15));
#17855=CARTESIAN_POINT('',(-0.0866025403784438,-0.4,-0.15));
#17856=CARTESIAN_POINT('',(0.0866025403784439,-0.64,-0.15));
#17857=CARTESIAN_POINT('Origin',(-0.173205080756888,-0.4,-2.77555756156289E-17));
#17858=CARTESIAN_POINT('',(-0.173205080756888,-0.4,-2.12115047744981E-17));
#17859=CARTESIAN_POINT('',(-0.0866025403784438,-0.4,-0.15));
#17860=CARTESIAN_POINT('',(-0.173205080756888,-0.64,-2.77555756156289E-17));
#17861=CARTESIAN_POINT('',(-0.173205080756888,-0.4,-2.12115047744981E-17));
#17862=CARTESIAN_POINT('',(-0.0866025403784438,-0.64,-0.15));
#17863=CARTESIAN_POINT('Origin',(-0.0866025403784439,-0.4,0.15));
#17864=CARTESIAN_POINT('',(-0.0866025403784439,-0.4,0.15));
#17865=CARTESIAN_POINT('',(-0.173205080756888,-0.4,-2.12115047744981E-17));
#17866=CARTESIAN_POINT('',(-0.0866025403784439,-0.64,0.15));
#17867=CARTESIAN_POINT('',(-0.0866025403784439,-0.4,0.15));
#17868=CARTESIAN_POINT('',(-0.173205080756888,-0.64,-2.12115047744981E-17));
#17869=CARTESIAN_POINT('Origin',(0.0866025403784439,-0.4,0.15));
#17870=CARTESIAN_POINT('',(0.0866025403784439,-0.4,0.15));
#17871=CARTESIAN_POINT('',(-0.0866025403784439,-0.4,0.15));
#17872=CARTESIAN_POINT('',(0.0866025403784439,-0.64,0.15));
#17873=CARTESIAN_POINT('',(0.0866025403784439,-0.4,0.15));
#17874=CARTESIAN_POINT('',(-0.0866025403784439,-0.64,0.15));
#17875=CARTESIAN_POINT('Origin',(0.173205080756888,-0.4,0.));
#17876=CARTESIAN_POINT('',(0.0866025403784439,-0.4,0.15));
#17877=CARTESIAN_POINT('',(0.0866025403784439,-0.64,0.15));
#17878=CARTESIAN_POINT('Origin',(0.,-0.4,-2.77555756156289E-17));
#17879=CARTESIAN_POINT('Origin',(0.,-0.64,-2.77555756156289E-17));
#53837=UNCERTAINTY_MEASURE_WITH_UNIT(LENGTH_MEASURE(0.001),#53910,
'DISTANCE_ACCURACY_VALUE',
'Maximum model space distance between geometric entities at asserted c
onnectivities');
#53859=UNCERTAINTY_MEASURE_WITH_UNIT(LENGTH_MEASURE(0.001),#53910,
'DISTANCE_ACCURACY_VALUE',
'Maximum model space distance between geometric entities at asserted c
onnectivities');
#53887=(
GEOMETRIC_REPRESENTATION_CONTEXT(3)
GLOBAL_UNCERTAINTY_ASSIGNED_CONTEXT((#53837))
GLOBAL_UNIT_ASSIGNED_CONTEXT((#53910,#53912,#53913))
REPRESENTATION_CONTEXT('','3D')
);
#53909=(
GEOMETRIC_REPRESENTATION_CONTEXT(3)
GLOBAL_UNCERTAINTY_ASSIGNED_CONTEXT((#53859))
GLOBAL_UNIT_ASSIGNED_CONTEXT((#53910,#53912,#53913))
REPRESENTATION_CONTEXT('','3D')
);
#53910=(
LENGTH_UNIT()
NAMED_UNIT(*)
SI_UNIT(.CENTI.,.METRE.)
);
#53912=(
NAMED_UNIT(*)
PLANE_ANGLE_UNIT()
SI_UNIT($,.RADIAN.)
);
#53913=(
NAMED_UNIT(*)
SI_UNIT($,.STERADIAN.)
SOLID_ANGLE_UNIT()
);
#53941=SHAPE_DEFINITION_REPRESENTATION(#54000,#54113);
#54000=PRODUCT_DEFINITION_SHAPE('',$,#54163);
#54113=SHAPE_REPRESENTATION('',(#12415),#53887);
#54135=PRODUCT_DEFINITION_CONTEXT('part definition',#54284,'design');
#54163=PRODUCT_DEFINITION('Cap Screw - M4x16','Cap Screw - M4x16',#54212,
#54135);
#54212=PRODUCT_DEFINITION_FORMATION('',$,#54313);
#54284=APPLICATION_CONTEXT(
'Core Data for Automotive Mechanical Design Process');
#54285=PRODUCT_CONTEXT('part definition',#54284,'mechanical');
#54313=PRODUCT('Cap Screw - M4x16','Cap Screw - M4x16',
'Cap Screw - M4x16',(#54285));
#54398=COLOUR_RGB('Black',0.12,0.14,0.17);
#54399=FILL_AREA_STYLE_COLOUR('',#54398);
#54400=FILL_AREA_STYLE('',(#54399));
#54401=SURFACE_STYLE_FILL_AREA(#54400);
#54402=SURFACE_SIDE_STYLE('',(#54401));
#54403=SURFACE_STYLE_USAGE(.BOTH.,#54402);
#54404=PRESENTATION_STYLE_ASSIGNMENT((#54403));
ENDSEC;
END-ISO-10303-21;
